ISO-10303-21;
HEADER;
/* Generated by software containing ST-Developer
 * from STEP Tools, Inc. (www.steptools.com) 
 */

FILE_DESCRIPTION(
/* description */ ('Cylinder foot and clevis mount kit'),
/* implementation_level */ '2;1');

FILE_NAME(
/* name */ 'Flat Washer - M5.step',
/* time_stamp */ '2026-10-27T20:10:43-07:00',
/* author */ (''),
/* organization */ (''),
/* preprocessor_version */ 'ST-DEVELOPER v20.2',
/* originating_system */ 'Autodesk Translation Framework v15.17.0.0',
/* authorisation */ '');

FILE_SCHEMA (('AUTOMOTIVE_DESIGN { 1 0 10303 214 3 1 1 }'));
ENDSEC;

DATA;
#10=MECHANICAL_DESIGN_GEOMETRIC_PRESENTATION_REPRESENTATION('',(#355),#9102);
#271=CONICAL_SURFACE('',#5670,0.275,0.785398163397449);
#299=SHAPE_REPRESENTATION_RELATIONSHIP('SRR','None',#9247,#327);
#327=ADVANCED_BREP_SHAPE_REPRESENTATION('',(#382),#9090);
#355=STYLED_ITEM('',(#9467),#382);
#382=MANIFOLD_SOLID_BREP('Body1',#4942);
#470=FACE_BOUND('',#1294,.T.);
#471=FACE_BOUND('',#1297,.T.);
#637=PLANE('',#5675);
#638=PLANE('',#5679);
#907=FACE_OUTER_BOUND('',#1291,.T.);
#908=FACE_OUTER_BOUND('',#1292,.T.);
#909=FACE_OUTER_BOUND('',#1293,.T.);
#910=FACE_OUTER_BOUND('',#1295,.T.);
#911=FACE_OUTER_BOUND('',#1296,.T.);
#1291=EDGE_LOOP('',(#4143,#4144,#4145,#4146));
#1292=EDGE_LOOP('',(#4147,#4148,#4149,#4150));
#1293=EDGE_LOOP('',(#4151));
#1294=EDGE_LOOP('',(#4152));
#1295=EDGE_LOOP('',(#4153,#4154,#4155,#4156));
#1296=EDGE_LOOP('',(#4157));
#1297=EDGE_LOOP('',(#4158));
#1652=LINE('',#8411,#2001);
#1653=LINE('',#8415,#2002);
#1654=LINE('',#8422,#2003);
#2001=VECTOR('',#6951,0.275);
#2002=VECTOR('',#6956,0.265);
#2003=VECTOR('',#6965,0.5);
#2266=CIRCLE('',#5671,0.285);
#2267=CIRCLE('',#5672,0.265);
#2268=CIRCLE('',#5674,0.265);
#2269=CIRCLE('',#5676,0.5);
#2270=CIRCLE('',#5678,0.5);
#2590=VERTEX_POINT('',#8408);
#2591=VERTEX_POINT('',#8410);
#2592=VERTEX_POINT('',#8414);
#2593=VERTEX_POINT('',#8418);
#2594=VERTEX_POINT('',#8421);
#3126=EDGE_CURVE('',#2590,#2590,#2266,.T.);
#3127=EDGE_CURVE('',#2590,#2591,#1652,.T.);
#3128=EDGE_CURVE('',#2591,#2591,#2267,.T.);
#3129=EDGE_CURVE('',#2591,#2592,#1653,.T.);
#3130=EDGE_CURVE('',#2592,#2592,#2268,.T.);
#3131=EDGE_CURVE('',#2593,#2593,#2269,.T.);
#3132=EDGE_CURVE('',#2593,#2594,#1654,.T.);
#3133=EDGE_CURVE('',#2594,#2594,#2270,.T.);
#4143=ORIENTED_EDGE('',*,*,#3126,.T.);
#4144=ORIENTED_EDGE('',*,*,#3127,.T.);
#4145=ORIENTED_EDGE('',*,*,#3128,.T.);
#4146=ORIENTED_EDGE('',*,*,#3127,.F.);
#4147=ORIENTED_EDGE('',*,*,#3128,.F.);
#4148=ORIENTED_EDGE('',*,*,#3129,.T.);
#4149=ORIENTED_EDGE('',*,*,#3130,.T.);
#4150=ORIENTED_EDGE('',*,*,#3129,.F.);
#4151=ORIENTED_EDGE('',*,*,#3131,.T.);
#4152=ORIENTED_EDGE('',*,*,#3126,.F.);
#4153=ORIENTED_EDGE('',*,*,#3131,.F.);
#4154=ORIENTED_EDGE('',*,*,#3132,.T.);
#4155=ORIENTED_EDGE('',*,*,#3133,.T.);
#4156=ORIENTED_EDGE('',*,*,#3132,.F.);
#4157=ORIENTED_EDGE('',*,*,#3133,.F.);
#4158=ORIENTED_EDGE('',*,*,#3130,.F.);
#4595=CYLINDRICAL_SURFACE('',#5673,0.265);
#4596=CYLINDRICAL_SURFACE('',#5677,0.5);
#4830=ADVANCED_FACE('',(#907),#271,.F.);
#4831=ADVANCED_FACE('',(#908),#4595,.F.);
#4832=ADVANCED_FACE('',(#909,#470),#637,.T.);
#4833=ADVANCED_FACE('',(#910),#4596,.T.);
#4834=ADVANCED_FACE('',(#911,#471),#638,.F.);
#4942=CLOSED_SHELL('',(#4830,#4831,#4832,#4833,#4834));
#5669=AXIS2_PLACEMENT_3D('',#8406,#6945,#6946);
#5670=AXIS2_PLACEMENT_3D('',#8407,#6947,#6948);
#5671=AXIS2_PLACEMENT_3D('',#8409,#6949,#6950);
#5672=AXIS2_PLACEMENT_3D('',#8412,#6952,#6953);
#5673=AXIS2_PLACEMENT_3D('',#8413,#6954,#6955);
#5674=AXIS2_PLACEMENT_3D('',#8416,#6957,#6958);
#5675=AXIS2_PLACEMENT_3D('',#8417,#6959,#6960);
#5676=AXIS2_PLACEMENT_3D('',#8419,#6961,#6962);
#5677=AXIS2_PLACEMENT_3D('',#8420,#6963,#6964);
#5678=AXIS2_PLACEMENT_3D('',#8423,#6966,#6967);
#5679=AXIS2_PLACEMENT_3D('',#8424,#6968,#6969);
#6945=DIRECTION('axis',(0.,0.,1.));
#6946=DIRECTION('refdir',(1.,0.,0.));
#6947=DIRECTION('center_axis',(0.,1.,0.));
#6948=DIRECTION('ref_axis',(1.,0.,0.));
#6949=DIRECTION('center_axis',(0.,1.,0.));
#6950=DIRECTION('ref_axis',(1.,0.,0.));
#6951=DIRECTION('',(0.707106781186548,-0.707106781186547,-8.65956056235494E-17));
#6952=DIRECTION('center_axis',(0.,-1.,0.));
#6953=DIRECTION('ref_axis',(1.,0.,0.));
#6954=DIRECTION('center_axis',(0.,1.,0.));
#6955=DIRECTION('ref_axis',(1.,0.,0.));
#6956=DIRECTION('',(0.,-1.,0.));
#6957=DIRECTION('center_axis',(0.,-1.,0.));
#6958=DIRECTION('ref_axis',(1.,0.,0.));
#6959=DIRECTION('center_axis',(0.,1.,0.));
#6960=DIRECTION('ref_axis',(1.,0.,0.));
#6961=DIRECTION('center_axis',(0.,1.,0.));
#6962=DIRECTION('ref_axis',(1.,0.,0.));
#6963=DIRECTION('center_axis',(0.,1.,0.));
#6964=DIRECTION('ref_axis',(1.,0.,0.));
#6965=DIRECTION('',(0.,-1.,0.));
#6966=DIRECTION('center_axis',(0.,1.,0.));
#6967=DIRECTION('ref_axis',(1.,0.,0.));
#6968=DIRECTION('center_axis',(0.,1.,0.));
#6969=DIRECTION('ref_axis',(1.,0.,0.));
#8406=CARTESIAN_POINT('',(0.,0.,0.));
#8407=CARTESIAN_POINT('Origin',(0.,0.09,0.));
#8408=CARTESIAN_POINT('',(-0.285,0.1,3.49024337756996E-17));
#8409=CARTESIAN_POINT('Origin',(0.,0.1,0.));
#8410=CARTESIAN_POINT('',(-0.265,0.08,-3.24531401774049E-17));
#8411=CARTESIAN_POINT('',(-0.275,0.09,3.36777869765522E-17));
#8412=CARTESIAN_POINT('Origin',(0.,0.08,0.));
#8413=CARTESIAN_POINT('Origin',(0.,0.,0.));
#8414=CARTESIAN_POINT('',(-0.265,0.,3.24531401774049E-17));
#8415=CARTESIAN_POINT('',(-0.265,0.,3.24531401774049E-17));
#8416=CARTESIAN_POINT('Origin',(0.,0.,0.));
#8417=CARTESIAN_POINT('Origin',(0.,0.1,0.));
#8418=CARTESIAN_POINT('',(-0.5,0.1,6.12323399573677E-17));
#8419=CARTESIAN_POINT('Origin',(0.,0.1,0.));
#8420=CARTESIAN_POINT('Origin',(0.,0.,0.));
#8421=CARTESIAN_POINT('',(-0.5,0.,6.12323399573677E-17));
#8422=CARTESIAN_POINT('',(-0.5,0.,6.12323399573677E-17));
#8423=CARTESIAN_POINT('Origin',(0.,0.,0.));
#8424=CARTESIAN_POINT('Origin',(0.,0.,0.));
#9057=UNCERTAINTY_MEASURE_WITH_UNIT(LENGTH_MEASURE(0.001),#9103,
'DISTANCE_ACCURACY_VALUE',
'Maximum model space distance between geometric entities at asserted c
onnectivities');
#9069=UNCERTAINTY_MEASURE_WITH_UNIT(LENGTH_MEASURE(0.001),#9103,
'DISTANCE_ACCURACY_VALUE',
'Maximum model space distance between geometric entities at asserted c
onnectivities');
#9090=(
GEOMETRIC_REPRESENTATION_CONTEXT(3)
GLOBAL_UNCERTAINTY_ASSIGNED_CONTEXT((#9057))
GLOBAL_UNIT_ASSIGNED_CONTEXT((#9103,#9105,#9106))
REPRESENTATION_CONTEXT('','3D')
);
#9102=(
GEOMETRIC_REPRESENTATION_CONTEXT(3)
GLOBAL_UNCERTAINTY_ASSIGNED_CONTEXT((#9069))
GLOBAL_UNIT_ASSIGNED_CONTEXT((#9103,#9105,#9106))
REPRESENTATION_CONTEXT('','3D')
);
#9103=(
LENGTH_UNIT()
NAMED_UNIT(*)
SI_UNIT(.CENTI.,.METRE.)
);
#9105=(
NAMED_UNIT(*)
PLANE_ANGLE_UNIT()
SI_UNIT($,.RADIAN.)
);
#9106=(
NAMED_UNIT(*)
SI_UNIT($,.STERADIAN.)
SOLID_ANGLE_UNIT()
);
#9127=SHAPE_DEFINITION_REPRESENTATION(#9161,#9247);
#9161=PRODUCT_DEFINITION_SHAPE('',$,#9280);
#9247=SHAPE_REPRESENTATION('',(#5669),#9090);
#9259=PRODUCT_DEFINITION_CONTEXT('part definition',#9357,'design');
#9280=PRODUCT_DEFINITION('Flat Washer - M5','Flat Washer - M5',#9312,#9259);
#9312=PRODUCT_DEFINITION_FORMATION('',$,#9379);
#9357=APPLICATION_CONTEXT(
'Core Data for Automotive Mechanical Design Process');
#9358=PRODUCT_CONTEXT('part definition',#9357,'mechanical');
#9379=PRODUCT('Flat Washer - M5','Flat Washer - M5','Flat Washer - M5',
(#9358));
#9461=COLOUR_RGB('Black',0.12,0.14,0.17);
#9462=FILL_AREA_STYLE_COLOUR('',#9461);
#9463=FILL_AREA_STYLE('',(#9462));
#9464=SURFACE_STYLE_FILL_AREA(#9463);
#9465=SURFACE_SIDE_STYLE('',(#9464));
#9466=SURFACE_STYLE_USAGE(.BOTH.,#9465);
#9467=PRESENTATION_STYLE_ASSIGNMENT((#9466));
ENDSEC;
END-ISO-10303-21;
